ISO-10303-21;
HEADER;
/* Generated by software containing ST-Developer
 * from STEP Tools, Inc. (www.steptools.com) 
 */

FILE_DESCRIPTION(
/* description */ ('PAT-097'),
/* implementation_level */ '2;1');

FILE_NAME(
/* name */ 'Stepped heel block.step',
/* time_stamp */ '2026-10-29T15:59:31-07:00',
/* author */ (''),
/* organization */ (''),
/* preprocessor_version */ 'ST-DEVELOPER v20.2',
/* originating_system */ 'Autodesk Translation Framework v15.17.0.0',
/* authorisation */ '');

FILE_SCHEMA (('AUTOMOTIVE_DESIGN { 1 0 10303 214 3 1 1 }'));
ENDSEC;

DATA;
#10=MECHANICAL_DESIGN_GEOMETRIC_PRESENTATION_REPRESENTATION('',(#77),#2768);
#63=SHAPE_REPRESENTATION_RELATIONSHIP('SRR','None',#2801,#70);
#70=ADVANCED_BREP_SHAPE_REPRESENTATION('',(#84),#2763);
#77=STYLED_ITEM('',(#2890),#84);
#84=MANIFOLD_SOLID_BREP('Body1',#1598);
#265=FACE_OUTER_BOUND('',#390,.T.);
#266=FACE_OUTER_BOUND('',#391,.T.);
#267=FACE_OUTER_BOUND('',#392,.T.);
#268=FACE_OUTER_BOUND('',#393,.T.);
#269=FACE_OUTER_BOUND('',#394,.T.);
#270=FACE_OUTER_BOUND('',#395,.T.);
#271=FACE_OUTER_BOUND('',#396,.T.);
#272=FACE_OUTER_BOUND('',#397,.T.);
#273=FACE_OUTER_BOUND('',#398,.T.);
#274=FACE_OUTER_BOUND('',#399,.T.);
#390=EDGE_LOOP('',(#1295,#1296,#1297,#1298));
#391=EDGE_LOOP('',(#1299,#1300,#1301,#1302));
#392=EDGE_LOOP('',(#1303,#1304,#1305,#1306));
#393=EDGE_LOOP('',(#1307,#1308,#1309,#1310));
#394=EDGE_LOOP('',(#1311,#1312,#1313,#1314));
#395=EDGE_LOOP('',(#1315,#1316,#1317,#1318));
#396=EDGE_LOOP('',(#1319,#1320,#1321,#1322));
#397=EDGE_LOOP('',(#1323,#1324,#1325,#1326));
#398=EDGE_LOOP('',(#1327,#1328,#1329,#1330,#1331,#1332,#1333,#1334));
#399=EDGE_LOOP('',(#1335,#1336,#1337,#1338,#1339,#1340,#1341,#1342));
#515=LINE('',#2543,#652);
#516=LINE('',#2545,#653);
#517=LINE('',#2547,#654);
#518=LINE('',#2548,#655);
#519=LINE('',#2551,#656);
#520=LINE('',#2553,#657);
#521=LINE('',#2554,#658);
#522=LINE('',#2557,#659);
#523=LINE('',#2559,#660);
#524=LINE('',#2560,#661);
#525=LINE('',#2563,#662);
#526=LINE('',#2565,#663);
#527=LINE('',#2566,#664);
#528=LINE('',#2569,#665);
#529=LINE('',#2571,#666);
#530=LINE('',#2572,#667);
#531=LINE('',#2575,#668);
#532=LINE('',#2577,#669);
#533=LINE('',#2578,#670);
#534=LINE('',#2581,#671);
#535=LINE('',#2583,#672);
#536=LINE('',#2584,#673);
#537=LINE('',#2586,#674);
#538=LINE('',#2587,#675);
#652=VECTOR('',#2102,1.);
#653=VECTOR('',#2103,1.);
#654=VECTOR('',#2104,1.);
#655=VECTOR('',#2105,1.);
#656=VECTOR('',#2108,1.);
#657=VECTOR('',#2109,1.);
#658=VECTOR('',#2110,1.);
#659=VECTOR('',#2113,1.);
#660=VECTOR('',#2114,1.);
#661=VECTOR('',#2115,1.);
#662=VECTOR('',#2118,1.);
#663=VECTOR('',#2119,1.);
#664=VECTOR('',#2120,1.);
#665=VECTOR('',#2123,1.);
#666=VECTOR('',#2124,1.);
#667=VECTOR('',#2125,1.);
#668=VECTOR('',#2128,1.);
#669=VECTOR('',#2129,1.);
#670=VECTOR('',#2130,1.);
#671=VECTOR('',#2133,1.);
#672=VECTOR('',#2134,1.);
#673=VECTOR('',#2135,1.);
#674=VECTOR('',#2138,1.);
#675=VECTOR('',#2139,1.);
#790=VERTEX_POINT('',#2541);
#791=VERTEX_POINT('',#2542);
#792=VERTEX_POINT('',#2544);
#793=VERTEX_POINT('',#2546);
#794=VERTEX_POINT('',#2550);
#795=VERTEX_POINT('',#2552);
#796=VERTEX_POINT('',#2556);
#797=VERTEX_POINT('',#2558);
#798=VERTEX_POINT('',#2562);
#799=VERTEX_POINT('',#2564);
#800=VERTEX_POINT('',#2568);
#801=VERTEX_POINT('',#2570);
#802=VERTEX_POINT('',#2574);
#803=VERTEX_POINT('',#2576);
#804=VERTEX_POINT('',#2580);
#805=VERTEX_POINT('',#2582);
#967=EDGE_CURVE('',#790,#791,#515,.T.);
#968=EDGE_CURVE('',#790,#792,#516,.T.);
#969=EDGE_CURVE('',#793,#792,#517,.T.);
#970=EDGE_CURVE('',#791,#793,#518,.T.);
#971=EDGE_CURVE('',#791,#794,#519,.T.);
#972=EDGE_CURVE('',#795,#793,#520,.T.);
#973=EDGE_CURVE('',#794,#795,#521,.T.);
#974=EDGE_CURVE('',#794,#796,#522,.T.);
#975=EDGE_CURVE('',#797,#795,#523,.T.);
#976=EDGE_CURVE('',#796,#797,#524,.T.);
#977=EDGE_CURVE('',#796,#798,#525,.T.);
#978=EDGE_CURVE('',#799,#797,#526,.T.);
#979=EDGE_CURVE('',#798,#799,#527,.T.);
#980=EDGE_CURVE('',#798,#800,#528,.T.);
#981=EDGE_CURVE('',#801,#799,#529,.T.);
#982=EDGE_CURVE('',#800,#801,#530,.T.);
#983=EDGE_CURVE('',#800,#802,#531,.T.);
#984=EDGE_CURVE('',#803,#801,#532,.T.);
#985=EDGE_CURVE('',#802,#803,#533,.T.);
#986=EDGE_CURVE('',#802,#804,#534,.T.);
#987=EDGE_CURVE('',#805,#803,#535,.T.);
#988=EDGE_CURVE('',#804,#805,#536,.T.);
#989=EDGE_CURVE('',#804,#790,#537,.T.);
#990=EDGE_CURVE('',#792,#805,#538,.T.);
#1295=ORIENTED_EDGE('',*,*,#967,.F.);
#1296=ORIENTED_EDGE('',*,*,#968,.T.);
#1297=ORIENTED_EDGE('',*,*,#969,.F.);
#1298=ORIENTED_EDGE('',*,*,#970,.F.);
#1299=ORIENTED_EDGE('',*,*,#971,.F.);
#1300=ORIENTED_EDGE('',*,*,#970,.T.);
#1301=ORIENTED_EDGE('',*,*,#972,.F.);
#1302=ORIENTED_EDGE('',*,*,#973,.F.);
#1303=ORIENTED_EDGE('',*,*,#974,.F.);
#1304=ORIENTED_EDGE('',*,*,#973,.T.);
#1305=ORIENTED_EDGE('',*,*,#975,.F.);
#1306=ORIENTED_EDGE('',*,*,#976,.F.);
#1307=ORIENTED_EDGE('',*,*,#977,.F.);
#1308=ORIENTED_EDGE('',*,*,#976,.T.);
#1309=ORIENTED_EDGE('',*,*,#978,.F.);
#1310=ORIENTED_EDGE('',*,*,#979,.F.);
#1311=ORIENTED_EDGE('',*,*,#980,.F.);
#1312=ORIENTED_EDGE('',*,*,#979,.T.);
#1313=ORIENTED_EDGE('',*,*,#981,.F.);
#1314=ORIENTED_EDGE('',*,*,#982,.F.);
#1315=ORIENTED_EDGE('',*,*,#983,.F.);
#1316=ORIENTED_EDGE('',*,*,#982,.T.);
#1317=ORIENTED_EDGE('',*,*,#984,.F.);
#1318=ORIENTED_EDGE('',*,*,#985,.F.);
#1319=ORIENTED_EDGE('',*,*,#986,.F.);
#1320=ORIENTED_EDGE('',*,*,#985,.T.);
#1321=ORIENTED_EDGE('',*,*,#987,.F.);
#1322=ORIENTED_EDGE('',*,*,#988,.F.);
#1323=ORIENTED_EDGE('',*,*,#989,.F.);
#1324=ORIENTED_EDGE('',*,*,#988,.T.);
#1325=ORIENTED_EDGE('',*,*,#990,.F.);
#1326=ORIENTED_EDGE('',*,*,#968,.F.);
#1327=ORIENTED_EDGE('',*,*,#990,.T.);
#1328=ORIENTED_EDGE('',*,*,#987,.T.);
#1329=ORIENTED_EDGE('',*,*,#984,.T.);
#1330=ORIENTED_EDGE('',*,*,#981,.T.);
#1331=ORIENTED_EDGE('',*,*,#978,.T.);
#1332=ORIENTED_EDGE('',*,*,#975,.T.);
#1333=ORIENTED_EDGE('',*,*,#972,.T.);
#1334=ORIENTED_EDGE('',*,*,#969,.T.);
#1335=ORIENTED_EDGE('',*,*,#989,.T.);
#1336=ORIENTED_EDGE('',*,*,#967,.T.);
#1337=ORIENTED_EDGE('',*,*,#971,.T.);
#1338=ORIENTED_EDGE('',*,*,#974,.T.);
#1339=ORIENTED_EDGE('',*,*,#977,.T.);
#1340=ORIENTED_EDGE('',*,*,#980,.T.);
#1341=ORIENTED_EDGE('',*,*,#983,.T.);
#1342=ORIENTED_EDGE('',*,*,#986,.T.);
#1483=PLANE('',#1772);
#1484=PLANE('',#1773);
#1485=PLANE('',#1774);
#1486=PLANE('',#1775);
#1487=PLANE('',#1776);
#1488=PLANE('',#1777);
#1489=PLANE('',#1778);
#1490=PLANE('',#1779);
#1491=PLANE('',#1780);
#1492=PLANE('',#1781);
#1558=ADVANCED_FACE('',(#265),#1483,.T.);
#1559=ADVANCED_FACE('',(#266),#1484,.T.);
#1560=ADVANCED_FACE('',(#267),#1485,.T.);
#1561=ADVANCED_FACE('',(#268),#1486,.T.);
#1562=ADVANCED_FACE('',(#269),#1487,.T.);
#1563=ADVANCED_FACE('',(#270),#1488,.T.);
#1564=ADVANCED_FACE('',(#271),#1489,.T.);
#1565=ADVANCED_FACE('',(#272),#1490,.T.);
#1566=ADVANCED_FACE('',(#273),#1491,.T.);
#1567=ADVANCED_FACE('',(#274),#1492,.F.);
#1598=CLOSED_SHELL('',(#1558,#1559,#1560,#1561,#1562,#1563,#1564,#1565,
#1566,#1567));
#1771=AXIS2_PLACEMENT_3D('',#2539,#2098,#2099);
#1772=AXIS2_PLACEMENT_3D('',#2540,#2100,#2101);
#1773=AXIS2_PLACEMENT_3D('',#2549,#2106,#2107);
#1774=AXIS2_PLACEMENT_3D('',#2555,#2111,#2112);
#1775=AXIS2_PLACEMENT_3D('',#2561,#2116,#2117);
#1776=AXIS2_PLACEMENT_3D('',#2567,#2121,#2122);
#1777=AXIS2_PLACEMENT_3D('',#2573,#2126,#2127);
#1778=AXIS2_PLACEMENT_3D('',#2579,#2131,#2132);
#1779=AXIS2_PLACEMENT_3D('',#2585,#2136,#2137);
#1780=AXIS2_PLACEMENT_3D('',#2588,#2140,#2141);
#1781=AXIS2_PLACEMENT_3D('',#2589,#2142,#2143);
#2098=DIRECTION('axis',(0.,0.,1.));
#2099=DIRECTION('refdir',(1.,0.,0.));
#2100=DIRECTION('center_axis',(-1.,0.,0.));
#2101=DIRECTION('ref_axis',(0.,0.,1.));
#2102=DIRECTION('',(0.,0.,-1.));
#2103=DIRECTION('',(0.,1.,0.));
#2104=DIRECTION('',(0.,0.,1.));
#2105=DIRECTION('',(0.,1.,0.));
#2106=DIRECTION('center_axis',(0.,0.,-1.));
#2107=DIRECTION('ref_axis',(-1.,0.,0.));
#2108=DIRECTION('',(1.,0.,0.));
#2109=DIRECTION('',(-1.,0.,0.));
#2110=DIRECTION('',(0.,1.,0.));
#2111=DIRECTION('center_axis',(1.,0.,0.));
#2112=DIRECTION('ref_axis',(0.,0.,-1.));
#2113=DIRECTION('',(0.,0.,1.));
#2114=DIRECTION('',(0.,0.,-1.));
#2115=DIRECTION('',(0.,1.,0.));
#2116=DIRECTION('center_axis',(0.,0.,1.));
#2117=DIRECTION('ref_axis',(1.,0.,0.));
#2118=DIRECTION('',(-1.,0.,0.));
#2119=DIRECTION('',(1.,0.,0.));
#2120=DIRECTION('',(0.,1.,0.));
#2121=DIRECTION('center_axis',(-1.,0.,0.));
#2122=DIRECTION('ref_axis',(0.,0.,1.));
#2123=DIRECTION('',(0.,0.,-1.));
#2124=DIRECTION('',(0.,0.,1.));
#2125=DIRECTION('',(0.,1.,0.));
#2126=DIRECTION('center_axis',(0.,0.,1.));
#2127=DIRECTION('ref_axis',(1.,0.,0.));
#2128=DIRECTION('',(-1.,0.,0.));
#2129=DIRECTION('',(1.,0.,0.));
#2130=DIRECTION('',(0.,1.,0.));
#2131=DIRECTION('center_axis',(-1.,0.,0.));
#2132=DIRECTION('ref_axis',(0.,0.,1.));
#2133=DIRECTION('',(0.,0.,-1.));
#2134=DIRECTION('',(0.,0.,1.));
#2135=DIRECTION('',(0.,1.,0.));
#2136=DIRECTION('center_axis',(0.,0.,1.));
#2137=DIRECTION('ref_axis',(1.,0.,0.));
#2138=DIRECTION('',(-1.,0.,0.));
#2139=DIRECTION('',(1.,0.,0.));
#2140=DIRECTION('center_axis',(0.,1.,0.));
#2141=DIRECTION('ref_axis',(0.,0.,1.));
#2142=DIRECTION('center_axis',(0.,1.,0.));
#2143=DIRECTION('ref_axis',(1.,0.,0.));
#2539=CARTESIAN_POINT('',(0.,0.,0.));
#2540=CARTESIAN_POINT('Origin',(2.,-1.5,1.4));
#2541=CARTESIAN_POINT('',(2.,-1.5,3.8));
#2542=CARTESIAN_POINT('',(2.,-1.5,1.4));
#2543=CARTESIAN_POINT('',(2.,-1.5,3.8));
#2544=CARTESIAN_POINT('',(2.,1.5,3.8));
#2545=CARTESIAN_POINT('',(2.,-1.5,3.8));
#2546=CARTESIAN_POINT('',(2.,1.5,1.4));
#2547=CARTESIAN_POINT('',(2.,1.5,3.8));
#2548=CARTESIAN_POINT('',(2.,-1.5,1.4));
#2549=CARTESIAN_POINT('Origin',(5.5,-1.5,1.4));
#2550=CARTESIAN_POINT('',(5.5,-1.5,1.4));
#2551=CARTESIAN_POINT('',(2.,-1.5,1.4));
#2552=CARTESIAN_POINT('',(5.5,1.5,1.4));
#2553=CARTESIAN_POINT('',(2.,1.5,1.4));
#2554=CARTESIAN_POINT('',(5.5,-1.5,1.4));
#2555=CARTESIAN_POINT('Origin',(5.5,-1.5,5.8));
#2556=CARTESIAN_POINT('',(5.5,-1.5,5.8));
#2557=CARTESIAN_POINT('',(5.5,-1.5,1.4));
#2558=CARTESIAN_POINT('',(5.5,1.5,5.8));
#2559=CARTESIAN_POINT('',(5.5,1.5,1.4));
#2560=CARTESIAN_POINT('',(5.5,-1.5,5.8));
#2561=CARTESIAN_POINT('Origin',(4.,-1.5,5.8));
#2562=CARTESIAN_POINT('',(4.,-1.5,5.8));
#2563=CARTESIAN_POINT('',(5.5,-1.5,5.8));
#2564=CARTESIAN_POINT('',(4.,1.5,5.8));
#2565=CARTESIAN_POINT('',(5.5,1.5,5.8));
#2566=CARTESIAN_POINT('',(4.,-1.5,5.8));
#2567=CARTESIAN_POINT('Origin',(4.,-1.5,4.8));
#2568=CARTESIAN_POINT('',(4.,-1.5,4.8));
#2569=CARTESIAN_POINT('',(4.,-1.5,5.8));
#2570=CARTESIAN_POINT('',(4.,1.5,4.8));
#2571=CARTESIAN_POINT('',(4.,1.5,5.8));
#2572=CARTESIAN_POINT('',(4.,-1.5,4.8));
#2573=CARTESIAN_POINT('Origin',(3.,-1.5,4.8));
#2574=CARTESIAN_POINT('',(3.,-1.5,4.8));
#2575=CARTESIAN_POINT('',(4.,-1.5,4.8));
#2576=CARTESIAN_POINT('',(3.,1.5,4.8));
#2577=CARTESIAN_POINT('',(4.,1.5,4.8));
#2578=CARTESIAN_POINT('',(3.,-1.5,4.8));
#2579=CARTESIAN_POINT('Origin',(3.,-1.5,3.8));
#2580=CARTESIAN_POINT('',(3.,-1.5,3.8));
#2581=CARTESIAN_POINT('',(3.,-1.5,4.8));
#2582=CARTESIAN_POINT('',(3.,1.5,3.8));
#2583=CARTESIAN_POINT('',(3.,1.5,4.8));
#2584=CARTESIAN_POINT('',(3.,-1.5,3.8));
#2585=CARTESIAN_POINT('Origin',(2.,-1.5,3.8));
#2586=CARTESIAN_POINT('',(3.,-1.5,3.8));
#2587=CARTESIAN_POINT('',(3.,1.5,3.8));
#2588=CARTESIAN_POINT('Origin',(3.75,1.5,3.6));
#2589=CARTESIAN_POINT('Origin',(3.75,-1.5,3.6));
#2754=UNCERTAINTY_MEASURE_WITH_UNIT(LENGTH_MEASURE(0.001),#2769,
'DISTANCE_ACCURACY_VALUE',
'Maximum model space distance between geometric entities at asserted c
onnectivities');
#2759=UNCERTAINTY_MEASURE_WITH_UNIT(LENGTH_MEASURE(0.001),#2769,
'DISTANCE_ACCURACY_VALUE',
'Maximum model space distance between geometric entities at asserted c
onnectivities');
#2763=(
GEOMETRIC_REPRESENTATION_CONTEXT(3)
GLOBAL_UNCERTAINTY_ASSIGNED_CONTEXT((#2754))
GLOBAL_UNIT_ASSIGNED_CONTEXT((#2769,#2771,#2772))
REPRESENTATION_CONTEXT('','3D')
);
#2768=(
GEOMETRIC_REPRESENTATION_CONTEXT(3)
GLOBAL_UNCERTAINTY_ASSIGNED_CONTEXT((#2759))
GLOBAL_UNIT_ASSIGNED_CONTEXT((#2769,#2771,#2772))
REPRESENTATION_CONTEXT('','3D')
);
#2769=(
LENGTH_UNIT()
NAMED_UNIT(*)
SI_UNIT(.CENTI.,.METRE.)
);
#2771=(
NAMED_UNIT(*)
PLANE_ANGLE_UNIT()
SI_UNIT($,.RADIAN.)
);
#2772=(
NAMED_UNIT(*)
SI_UNIT($,.STERADIAN.)
SOLID_ANGLE_UNIT()
);
#2776=SHAPE_DEFINITION_REPRESENTATION(#2784,#2801);
#2784=PRODUCT_DEFINITION_SHAPE('',$,#2810);
#2801=SHAPE_REPRESENTATION('',(#1771),#2763);
#2806=PRODUCT_DEFINITION_CONTEXT('part definition',#2832,'design');
#2810=PRODUCT_DEFINITION('Stepped heel block',
'Stepped heel block',#2818,#2806);
#2818=PRODUCT_DEFINITION_FORMATION('',$,#2837);
#2832=APPLICATION_CONTEXT(
'Core Data for Automotive Mechanical Design Process');
#2833=PRODUCT_CONTEXT('part definition',#2832,'mechanical');
#2837=PRODUCT('Stepped heel block','Stepped heel block',
'Stepped heel block',(#2833));
#2884=COLOUR_RGB('Dark Blue',0.08,0.2,0.34);
#2885=FILL_AREA_STYLE_COLOUR('',#2884);
#2886=FILL_AREA_STYLE('',(#2885));
#2887=SURFACE_STYLE_FILL_AREA(#2886);
#2888=SURFACE_SIDE_STYLE('',(#2887));
#2889=SURFACE_STYLE_USAGE(.BOTH.,#2888);
#2890=PRESENTATION_STYLE_ASSIGNMENT((#2889));
ENDSEC;
END-ISO-10303-21;
